ISO-10303-21;
HEADER;
FILE_DESCRIPTION (('STEP AP214'),
    '1' );
FILE_NAME ('Bolt.step',
    '2026-10-06T08:09:25',
    ( '' ),
    ( '' ),
    'SwSTEP 2.0',
    'SolidWorks 2021',
    '' );
FILE_SCHEMA (( 'AUTOMOTIVE_DESIGN' ));
ENDSEC;

DATA;
#10=PRODUCT_DEFINITION_FORMATION_WITH_SPECIFIED_SOURCE ( 'ANY', '', #19447, .NOT_KNOWN. ) ;
#95=CARTESIAN_POINT ( 'NONE',  ( 5.213674118230995802, -0.7499999999999382716, -1.500000000000001332 ) ) ;
#157=CARTESIAN_POINT ( 'NONE',  ( 4.560256354962182179, -0.7499999999999382716, -2.508007965330665723 ) ) ;
#168=ORIENTED_EDGE ( 'NONE', *, *, #3680, .T. ) ;
#182=DIRECTION ( 'NONE',  ( -0.7071067811865435759, 2.143845182814170115E-16, -0.7071067811865514585 ) ) ;
#286=( NAMED_UNIT ( * ) PLANE_ANGLE_UNIT ( ) SI_UNIT ( $, .RADIAN. ) );
#389=FACE_OUTER_BOUND ( 'NONE', #20121, .T. ) ;
#408=DIRECTION ( 'NONE',  ( -7.860214984770699307E-18, 1.409037165336591006E-16, 1.000000000000000000 ) ) ;
#439=DIRECTION ( 'NONE',  ( -1.000000000000000000, 9.325873406851321250E-15, 0.000000000000000000 ) ) ;
#500=COLOUR_RGB ( '', 0.66274510, 0.83137255, 0.94901961) ;
#502=CIRCLE ( 'NONE', #2759, 2.249999999999996003 ) ;
#551=AXIS2_PLACEMENT_3D ( 'NONE', #11797, #15781, #13457 ) ;
#584=CARTESIAN_POINT ( 'NONE',  ( 3.806148720138569086, 0.7500000000000555112, -3.000000000000023093 ) ) ;
#619=AXIS2_PLACEMENT_3D ( 'NONE', #4316, #2093, #7863 ) ;
#634=DIRECTION ( 'NONE',  ( -1.000000000000000000, 4.440892098500650814E-16, 7.860214984771115307E-18 ) ) ;
#697=CARTESIAN_POINT ( 'NONE',  ( 2.250000000000001776, 2.697410439246579483E-14, 17.49999999999997513 ) ) ;
#699=AXIS2_PLACEMENT_3D ( 'NONE', #5072, #17177, #13549 ) ;
#744=ORIENTED_EDGE ( 'NONE', *, *, #11852, .F. ) ;
#749=VERTEX_POINT ( 'NONE', #21648 ) ;
#886=( NAMED_UNIT ( * ) PLANE_ANGLE_UNIT ( ) SI_UNIT ( $, .RADIAN. ) );
#919=VERTEX_POINT ( 'NONE', #697 ) ;
#950=EDGE_CURVE ( 'NONE', #17683, #6944, #7745, .T. ) ;
#955=VERTEX_POINT ( 'NONE', #16777 ) ;
#1040=ORIENTED_EDGE ( 'NONE', *, *, #18309, .F. ) ;
#1195=CARTESIAN_POINT ( 'NONE',  ( 1.387778780781445676E-14, 4.857225732735059864E-14, -1.500000000000001332 ) ) ;
#1197=CARTESIAN_POINT ( 'NONE',  ( -4.690415759823443942, 0.7500000000000770495, -2.000000000000001776 ) ) ;
#1208=ORIENTED_EDGE ( 'NONE', *, *, #21026, .T. ) ;
#1300=ORIENTED_EDGE ( 'NONE', *, *, #4213, .F. ) ;
#1317=CARTESIAN_POINT ( 'NONE',  ( -4.182780094295433848, 0.7500000000000507372, -2.876053189442132396 ) ) ;
#1371=EDGE_CURVE ( 'NONE', #5959, #11179, #15659, .T. ) ;
#1395=LINE ( 'NONE', #22932, #3517 ) ;
#1423=AXIS2_PLACEMENT_3D ( 'NONE', #8985, #5458, #16483 ) ;
#1445=PLANE ( 'NONE',  #551 ) ;
#1543=ORIENTED_EDGE ( 'NONE', *, *, #22186, .F. ) ;
#1579=AXIS2_PLACEMENT_3D ( 'NONE', #17020, #4198, #13042 ) ;
#1637=AXIS2_PLACEMENT_3D ( 'NONE', #21705, #18178, #9458 ) ;
#1671=AXIS2_PLACEMENT_3D ( 'NONE', #14122, #21310, #19533 ) ;
#1678=DIRECTION ( 'NONE',  ( 7.860214984770699307E-18, -1.409037165336591006E-16, -1.000000000000000000 ) ) ;
#1680=CARTESIAN_POINT ( 'NONE',  ( 4.484612144975566039, -0.7499999999999384936, -2.618262478605820398 ) ) ;
#1687=EDGE_CURVE ( 'NONE', #19077, #4132, #10111, .T. ) ;
#1706=CARTESIAN_POINT ( 'NONE',  ( 0.000000000000000000, 0.000000000000000000, 0.000000000000000000 ) ) ;
#1716=ORIENTED_EDGE ( 'NONE', *, *, #12803, .F. ) ;
#1921=( NAMED_UNIT ( * ) SI_UNIT ( $, .STERADIAN. ) SOLID_ANGLE_UNIT ( ) );
#1972=ORIENTED_EDGE ( 'NONE', *, *, #18954, .F. ) ;
#2043=SURFACE_STYLE_USAGE ( .BOTH. , #21820 ) ;
#2093=DIRECTION ( 'NONE',  ( -7.860214984770699307E-18, 1.409037165336591006E-16, 1.000000000000000000 ) ) ;
#2133=CYLINDRICAL_SURFACE ( 'NONE', #17520, 4.749999999999986677 ) ;
#2184=ORIENTED_EDGE ( 'NONE', *, *, #17433, .F. ) ;
#2266=UNCERTAINTY_MEASURE_WITH_UNIT (LENGTH_MEASURE( 1.000000000000000082E-05 ), #14864, 'distance_accuracy_value', 'NONE');
#2383=ORIENTED_EDGE ( 'NONE', *, *, #4311, .T. ) ;
#2495=EDGE_LOOP ( 'NONE', ( #7906, #19985, #5114, #4922 ) ) ;
#2712=SURFACE_STYLE_USAGE ( .BOTH. , #15184 ) ;
#2747=DIRECTION ( 'NONE',  ( 7.860214984770699307E-18, -1.409037165336591006E-16, -1.000000000000000000 ) ) ;
#2752=PRODUCT_DEFINITION_CONTEXT ( 'detailed design', #16293, 'design' ) ;
#2759=AXIS2_PLACEMENT_3D ( 'NONE', #22819, #3293, #7175 ) ;
#2798=AXIS2_PLACEMENT_3D ( 'NONE', #8527, #19461, #4990 ) ;
#2813=DIRECTION ( 'NONE',  ( -7.860214984770699307E-18, 1.409037165336591006E-16, 1.000000000000000000 ) ) ;
#2912=DIRECTION ( 'NONE',  ( 7.860214984770699307E-18, -1.409037165336591006E-16, -1.000000000000000000 ) ) ;
#2963=DIRECTION ( 'NONE',  ( 0.000000000000000000, 0.000000000000000000, 1.000000000000000000 ) ) ;
#2996=( NAMED_UNIT ( * ) PLANE_ANGLE_UNIT ( ) SI_UNIT ( $, .RADIAN. ) );
#3015=DIRECTION ( 'NONE',  ( -7.860214984770699307E-18, 1.409037165336591006E-16, 1.000000000000000000 ) ) ;
#3032=FACE_OUTER_BOUND ( 'NONE', #7451, .T. ) ;
#3073=CARTESIAN_POINT ( 'NONE',  ( -4.663920683512478682, 0.7500000000000504041, -2.263176076085167132 ) ) ;
#3111=MECHANICAL_DESIGN_GEOMETRIC_PRESENTATION_REPRESENTATION('',(#6872),#12107);
#3170=CARTESIAN_POINT ( 'NONE',  ( 4.749999999999986677, -2.109423746787803343E-15, -3.733602117766269525E-17 ) ) ;
#3179=LINE ( 'NONE', #14226, #13647 ) ;
#3209=ORIENTED_EDGE ( 'NONE', *, *, #3680, .F. ) ;
#3218=DIRECTION ( 'NONE',  ( -1.000000000000000000, 4.440892098500637995E-16, 0.000000000000000000 ) ) ;
#3242=ORIENTED_EDGE ( 'NONE', *, *, #14791, .T. ) ;
#3293=DIRECTION ( 'NONE',  ( -7.860214984770699307E-18, 1.409037165336591006E-16, 1.000000000000000000 ) ) ;
#3305=DIRECTION ( 'NONE',  ( -6.106226635438366889E-16, 1.000000000000000000, -1.409037165336591006E-16 ) ) ;
#3316=( NAMED_UNIT ( * ) PLANE_ANGLE_UNIT ( ) SI_UNIT ( $, .RADIAN. ) );
#3334=CARTESIAN_POINT ( 'NONE',  ( 4.690415759823464370, -0.7499999999999383826, -2.131890305193608448 ) ) ;
#3367=COLOUR_RGB ( '', 0.72549020, 0.75294118, 0.79215686) ;
#3385=ORIENTED_EDGE ( 'NONE', *, *, #13961, .T. ) ;
#3456=VERTEX_POINT ( 'NONE', #8333 ) ;
#3517=VECTOR ( 'NONE', #15735, 1000.000000000000000 ) ;
#3644=CARTESIAN_POINT ( 'NONE',  ( 4.690415759823415520, 0.7500000000000770495, -1.500000000000001332 ) ) ;
#3659=EDGE_LOOP ( 'NONE', ( #7424, #4140, #168, #20300, #7938, #21930 ) ) ;
#3680=EDGE_CURVE ( 'NONE', #17683, #23243, #6082, .T. ) ;
#3748=FACE_OUTER_BOUND ( 'NONE', #15860, .T. ) ;
#3756=LINE ( 'NONE', #8837, #14917 ) ;
#3827=EDGE_CURVE ( 'NONE', #21586, #749, #19124, .T. ) ;
#3848=AXIS2_PLACEMENT_3D ( 'NONE', #9661, #4126, #9321 ) ;
#4013=( NAMED_UNIT ( * ) SI_UNIT ( $, .STERADIAN. ) SOLID_ANGLE_UNIT ( ) );
#4029=VERTEX_POINT ( 'NONE', #14302 ) ;
#4037=FILL_AREA_STYLE ('',( #17938 ) ) ;
#4052=EDGE_CURVE ( 'NONE', #3456, #10401, #10761, .T. ) ;
#4057=ORIENTED_EDGE ( 'NONE', *, *, #5652, .F. ) ;
#4085=ORIENTED_EDGE ( 'NONE', *, *, #10217, .F. ) ;
#4098=CARTESIAN_POINT ( 'NONE',  ( 3.674234614174737068, 0.7500000000000492939, -3.000000000000002665 ) ) ;
#4099=DIRECTION ( 'NONE',  ( -1.000000000000000000, 4.440892098500650814E-16, 7.860214984771115307E-18 ) ) ;
#4123=CYLINDRICAL_SURFACE ( 'NONE', #16208, 4.749999999999986677 ) ;
#4126=DIRECTION ( 'NONE',  ( 7.860214984770699307E-18, -1.409037165336591006E-16, -1.000000000000000000 ) ) ;
#4132=VERTEX_POINT ( 'NONE', #18634 ) ;
#4140=ORIENTED_EDGE ( 'NONE', *, *, #8474, .F. ) ;
#4198=DIRECTION ( 'NONE',  ( 7.860214984771176937E-18, 1.409037165336591006E-16, 1.000000000000000000 ) ) ;
#4210=CARTESIAN_POINT ( 'NONE',  ( -3.674234614174765046, 0.7500000000000630607, -2.999999999999995559 ) ) ;
#4213=EDGE_CURVE ( 'NONE', #6944, #21173, #6407, .T. ) ;
#4234=( GEOMETRIC_REPRESENTATION_CONTEXT ( 3 ) GLOBAL_UNCERTAINTY_ASSIGNED_CONTEXT ( ( #2266 ) ) GLOBAL_UNIT_ASSIGNED_CONTEXT ( ( #14864, #286, #1921 ) ) REPRESENTATION_CONTEXT ( 'NONE', 'WORKASPACE' ) );
#4241=FACE_OUTER_BOUND ( 'NONE', #14857, .T. ) ;
#4311=EDGE_CURVE ( 'NONE', #5959, #11179, #18690, .T. ) ;
#4316=CARTESIAN_POINT ( 'NONE',  ( 1.387778780781445676E-14, 4.857225732735059864E-14, -1.500000000000001332 ) ) ;
#4322=CARTESIAN_POINT ( 'NONE',  ( 4.690415759823415520, 0.7500000000000700551, -2.000000000000001776 ) ) ;
#4370=CARTESIAN_POINT ( 'NONE',  ( 5.213674118230995802, -0.7499999999999382716, -1.500000000000001332 ) ) ;
#4384=CARTESIAN_POINT ( 'NONE',  ( -2.500000000000000000, 2.761527815601788505E-14, 17.24999999999997513 ) ) ;
#4502=CARTESIAN_POINT ( 'NONE',  ( 1.387778780781445676E-14, 4.857225732735059864E-14, -1.500000000000001332 ) ) ;
#4506=ADVANCED_FACE ( 'NONE', ( #389 ), #2133, .T. ) ;
#4540=DIRECTION ( 'NONE',  ( 1.000000000000000000, -4.440892098500655744E-16, 7.860214984770760936E-18 ) ) ;
#4722=EDGE_CURVE ( 'NONE', #14397, #19077, #21323, .T. ) ;
#4922=ORIENTED_EDGE ( 'NONE', *, *, #23030, .F. ) ;
#4943=CARTESIAN_POINT ( 'NONE',  ( 0.000000000000000000, 0.000000000000000000, 0.000000000000000000 ) ) ;
#4990=DIRECTION ( 'NONE',  ( 1.000000000000000000, -4.440892098500650814E-16, -7.860214984771113767E-18 ) ) ;
#5072=CARTESIAN_POINT ( 'NONE',  ( 0.000000000000000000, 2.775557561562891351E-14, 17.49999999999997513 ) ) ;
#5114=ORIENTED_EDGE ( 'NONE', *, *, #16858, .F. ) ;
#5263=VERTEX_POINT ( 'NONE', #4384 ) ;
#5306=DIRECTION ( 'NONE',  ( 1.000000000000000000, 0.000000000000000000, 0.000000000000000000 ) ) ;
#5442=AXIS2_PLACEMENT_3D ( 'NONE', #1195, #18959, #20957 ) ;
#5458=DIRECTION ( 'NONE',  ( -7.860214984770699307E-18, 1.409037165336591006E-16, 1.000000000000000000 ) ) ;
#5497=PLANE ( 'NONE',  #19245 ) ;
#5532=PLANE ( 'NONE',  #7275 ) ;
#5542=MANIFOLD_SOLID_BREP ( 'Chamfer1', #15926 ) ;
#5548=ORIENTED_EDGE ( 'NONE', *, *, #5782, .F. ) ;
#5591=EDGE_CURVE ( 'NONE', #5263, #16755, #11349, .T. ) ;
#5652=EDGE_CURVE ( 'NONE', #919, #16755, #10234, .T. ) ;
#5685=DIRECTION ( 'NONE',  ( 1.000000000000000000, -4.440892098500654758E-16, 0.000000000000000000 ) ) ;
#5741=CARTESIAN_POINT ( 'NONE',  ( -3.674234614174765046, -0.7499999999999451550, -3.000000000000051070 ) ) ;
#5782=EDGE_CURVE ( 'NONE', #6059, #9570, #22475, .T. ) ;
#5805=( NAMED_UNIT ( * ) PLANE_ANGLE_UNIT ( ) SI_UNIT ( $, .RADIAN. ) );
#5896=ORIENTED_EDGE ( 'NONE', *, *, #11876, .F. ) ;
#5907=DIRECTION ( 'NONE',  ( -7.860214984770699307E-18, 1.409037165336591006E-16, 1.000000000000000000 ) ) ;
#5941=B_SPLINE_CURVE_WITH_KNOTS ( 'NONE', 3,
 ( #14265, #3334, #15893, #157, #1680, #22978, #19678, #10842, #7106, #21454 ),
 .UNSPECIFIED., .F., .F.,
 ( 4, 2, 2, 2, 4 ),
 ( 0.003632676470446334280, 0.004026789025884817963, 0.004420901581323301646, 0.004815014136761786197, 0.005209126692200269880 ),
 .UNSPECIFIED. ) ;
#5950=EDGE_LOOP ( 'NONE', ( #2383, #7232 ) ) ;
#5959=VERTEX_POINT ( 'NONE', #4210 ) ;
#5993=FACE_OUTER_BOUND ( 'NONE', #13842, .T. ) ;
#5997=CARTESIAN_POINT ( 'NONE',  ( 4.560724896783636240, 0.7500000000000559552, -2.506869887779819450 ) ) ;
#6008=AXIS2_PLACEMENT_3D ( 'NONE', #7744, #14804, #20894 ) ;
#6017=CARTESIAN_POINT ( 'NONE',  ( -3.805981007006675298, -0.7499999999999436007, -3.000000000000016875 ) ) ;
#6059=VERTEX_POINT ( 'NONE', #20115 ) ;
#6082=LINE ( 'NONE', #22082, #13071 ) ;
#6108=CARTESIAN_POINT ( 'NONE',  ( 3.938635139691124998, 0.7500000000000556222, -2.974447373137671047 ) ) ;
#6117=VECTOR ( 'NONE', #19069, 999.9999999999998863 ) ;
#6269=UNCERTAINTY_MEASURE_WITH_UNIT (LENGTH_MEASURE( 1.000000000000000082E-05 ), #14842, 'distance_accuracy_value', 'NONE');
#6297=SURFACE_STYLE_FILL_AREA ( #9709 ) ;
#6341=AXIS2_PLACEMENT_3D ( 'NONE', #22489, #6376, #15762 ) ;
#6375=PLANE ( 'NONE',  #5442 ) ;
#6376=DIRECTION ( 'NONE',  ( -7.860214984770699307E-18, 1.409037165336591006E-16, 1.000000000000000000 ) ) ;
#6377=CARTESIAN_POINT ( 'NONE',  ( -4.483790972161962429, 0.7500000000000504041, -2.619109171265773917 ) ) ;
#6383=CARTESIAN_POINT ( 'NONE',  ( 1.387778780781445676E-14, 4.857225732735059864E-14, -1.500000000000001332 ) ) ;
#6407=LINE ( 'NONE', #22284, #19079 ) ;
#6484=CARTESIAN_POINT ( 'NONE',  ( -4.560231799112663964, 0.7500000000000501821, -2.508055037556191635 ) ) ;
#6495=EDGE_LOOP ( 'NONE', ( #7832, #19526, #1543, #12714, #17961, #8028 ) ) ;
#6604=CARTESIAN_POINT ( 'NONE',  ( -3.938125153161836423, 0.7500000000000509592, -2.974627600405583383 ) ) ;
#6810=DIRECTION ( 'NONE',  ( -7.860214984770699307E-18, 1.409037165336591006E-16, 1.000000000000000000 ) ) ;
#6835=ADVANCED_FACE ( 'NONE', ( #4241 ), #9782, .T. ) ;
#6872=STYLED_ITEM ( 'NONE', ( #21908 ), #5542 ) ;
#6920=AXIS2_PLACEMENT_3D ( 'NONE', #17011, #2912, #15373 ) ;
#6944=VERTEX_POINT ( 'NONE', #11889 ) ;
#6953=ADVANCED_BREP_SHAPE_REPRESENTATION ( '', ( #5542, #22115 ), #22911 ) ;
#6965=DIRECTION ( 'NONE',  ( 7.860214984770699307E-18, -1.409037165336591006E-16, -1.000000000000000000 ) ) ;
#7009=FACE_OUTER_BOUND ( 'NONE', #5950, .T. ) ;
#7106=CARTESIAN_POINT ( 'NONE',  ( 3.805574971170883281, -0.7499999999999388267, -3.000000000000007994 ) ) ;
#7175=DIRECTION ( 'NONE',  ( 1.000000000000000000, -4.440892098500651800E-16, 0.000000000000000000 ) ) ;
#7232=ORIENTED_EDGE ( 'NONE', *, *, #1371, .F. ) ;
#7275=AXIS2_PLACEMENT_3D ( 'NONE', #14235, #3305, #17881 ) ;
#7321=VERTEX_POINT ( 'NONE', #20704 ) ;
#7323=VECTOR ( 'NONE', #21073, 1000.000000000000000 ) ;
#7424=ORIENTED_EDGE ( 'NONE', *, *, #11852, .T. ) ;
#7451=EDGE_LOOP ( 'NONE', ( #4057, #10408, #21362, #19699 ) ) ;
#7455=UNCERTAINTY_MEASURE_WITH_UNIT (LENGTH_MEASURE( 1.000000000000000082E-05 ), #17648, 'distance_accuracy_value', 'NONE');
#7616=VECTOR ( 'NONE', #634, 1000.000000000000000 ) ;
#7630=AXIS2_PLACEMENT_3D ( 'NONE', #16271, #408, #9345 ) ;
#7744=CARTESIAN_POINT ( 'NONE',  ( 1.387778780781445676E-14, 4.163336342344337027E-14, -2.000000000000001776 ) ) ;
#7745=CIRCLE ( 'NONE', #619, 4.749999999999986677 ) ;
#7792=ORIENTED_EDGE ( 'NONE', *, *, #18954, .T. ) ;
#7812=STYLED_ITEM ( 'NONE', ( #22379 ), #6835 ) ;
#7832=ORIENTED_EDGE ( 'NONE', *, *, #8474, .T. ) ;
#7863=DIRECTION ( 'NONE',  ( -1.000000000000000000, 4.440892098500654758E-16, 0.000000000000000000 ) ) ;
#7906=ORIENTED_EDGE ( 'NONE', *, *, #1687, .F. ) ;
#7938=ORIENTED_EDGE ( 'NONE', *, *, #17433, .T. ) ;
#7995=ORIENTED_EDGE ( 'NONE', *, *, #18309, .T. ) ;
#7999=CIRCLE ( 'NONE', #13255, 2.499999999999993339 ) ;
#8009=CARTESIAN_POINT ( 'NONE',  ( -4.580466231768955510, -0.7499999999999442668, -2.524719371073009810 ) ) ;
#8028=ORIENTED_EDGE ( 'NONE', *, *, #950, .F. ) ;
#8054=FILL_AREA_STYLE_COLOUR ( '', #3367 ) ;
#8075=DIRECTION ( 'NONE',  ( -7.860214984770699307E-18, 1.409037165336591006E-16, 1.000000000000000000 ) ) ;
#8171=PRESENTATION_STYLE_ASSIGNMENT (( #20995 ) ) ;
#8249=DIRECTION ( 'NONE',  ( 7.860214984770699307E-18, -1.409037165336591006E-16, -1.000000000000000000 ) ) ;
#8333=CARTESIAN_POINT ( 'NONE',  ( -4.690415759823443942, 0.7500000000000770495, -1.500000000000001332 ) ) ;
#8351=ORIENTED_EDGE ( 'NONE', *, *, #22186, .T. ) ;
#8412=( LENGTH_UNIT ( ) NAMED_UNIT ( * ) SI_UNIT ( .MILLI., .METRE. ) );
#8474=EDGE_CURVE ( 'NONE', #17683, #955, #9453, .T. ) ;
#8527=CARTESIAN_POINT ( 'NONE',  ( 4.163336342344337027E-14, 3.469446951953614189E-14, -3.000000000000002665 ) ) ;
#8711=FACE_OUTER_BOUND ( 'NONE', #21782, .T. ) ;
#8732=CARTESIAN_POINT ( 'NONE',  ( 5.213674118230995802, 0.7500000000000492939, -3.000000000000002665 ) ) ;
#8795=CONICAL_SURFACE ( 'NONE', #6920, 2.249999999999996003, 0.7853981633974439491 ) ;
#8837=CARTESIAN_POINT ( 'NONE',  ( -4.690415759823429731, 0.7500000000000630607, -3.000000000000002665 ) ) ;
#8879=DIRECTION ( 'NONE',  ( -7.860214984770699307E-18, 1.409037165336591006E-16, 1.000000000000000000 ) ) ;
#8985=CARTESIAN_POINT ( 'NONE',  ( 1.387778780781445676E-14, 4.163336342344337027E-14, -2.000000000000001776 ) ) ;
#9057=AXIS2_PLACEMENT_3D ( 'NONE', #9840, #11708, #18899 ) ;
#9107=CARTESIAN_POINT ( 'NONE',  ( -2.249999999999996003, 2.875477633779155440E-14, 17.49999999999997513 ) ) ;
#9121=COLOUR_RGB ( '', 0.72549020, 0.75294118, 0.79215686) ;
#9203=DIRECTION ( 'NONE',  ( -7.860214984770699307E-18, 1.409037165336591006E-16, 1.000000000000000000 ) ) ;
#9321=DIRECTION ( 'NONE',  ( 1.000000000000000000, -5.773159728050815588E-15, 0.000000000000000000 ) ) ;
#9336=ORIENTED_EDGE ( 'NONE', *, *, #16840, .T. ) ;
#9345=DIRECTION ( 'NONE',  ( 1.000000000000000000, -4.440892098500650814E-16, -7.860214984771115307E-18 ) ) ;
#9410=LINE ( 'NONE', #16554, #17794 ) ;
#9453=LINE ( 'NONE', #4370, #7616 ) ;
#9456=ORIENTED_EDGE ( 'NONE', *, *, #23030, .T. ) ;
#9458=DIRECTION ( 'NONE',  ( -1.000000000000000000, 4.440892098500641939E-16, 0.000000000000000000 ) ) ;
#9535=ORIENTED_EDGE ( 'NONE', *, *, #4052, .F. ) ;
#9566=VECTOR ( 'NONE', #182, 999.9999999999998863 ) ;
#9570=VERTEX_POINT ( 'NONE', #10780 ) ;
#9595=AXIS2_PLACEMENT_3D ( 'NONE', #18931, #2813, #18684 ) ;
#9631=CARTESIAN_POINT ( 'NONE',  ( 4.690415759823449271, 0.7500000000000559552, -2.132316638858528624 ) ) ;
#9661=CARTESIAN_POINT ( 'NONE',  ( 0.000000000000000000, 1.387778780781445676E-14, 17.24999999999997513 ) ) ;
#9666=FILL_AREA_STYLE ('',( #11304 ) ) ;
#9709=FILL_AREA_STYLE ('',( #8054 ) ) ;
#9770=ADVANCED_FACE ( 'NONE', ( #11124 ), #5497, .F. ) ;
#9782=CYLINDRICAL_SURFACE ( 'NONE', #699, 2.499999999999993339 ) ;
#9784=DIRECTION ( 'NONE',  ( -1.000000000000000000, 1.025846074753645022E-13, 0.000000000000000000 ) ) ;
#9818=( NAMED_UNIT ( * ) SI_UNIT ( $, .STERADIAN. ) SOLID_ANGLE_UNIT ( ) );
#9840=CARTESIAN_POINT ( 'NONE',  ( 1.387778780781445676E-14, 4.163336342344337027E-14, -2.000000000000001776 ) ) ;
#10016=CARTESIAN_POINT ( 'NONE',  ( 2.249999999999996003, 2.703192042327442355E-14, 17.49999999999997513 ) ) ;
#10028=EDGE_CURVE ( 'NONE', #9570, #6059, #7999, .T. ) ;
#10049=PRODUCT_DEFINITION_SHAPE ( 'NONE', 'NONE',  #20122 ) ;
#10050=ORIENTED_EDGE ( 'NONE', *, *, #20890, .T. ) ;
#10080=MECHANICAL_DESIGN_GEOMETRIC_PRESENTATION_REPRESENTATION('',(#7812),#20230);
#10111=B_SPLINE_CURVE_WITH_KNOTS ( 'NONE', 3,
 ( #18600, #6017, #18370, #13421, #15174, #8009, #22368, #20131 ),
 .UNSPECIFIED., .F., .F.,
 ( 4, 2, 2, 4 ),
 ( 0.005324102488572167793, 0.005718019702363091698, 0.006111936916154015603, 0.006899771343735862546 ),
 .UNSPECIFIED. ) ;
#10142=ORIENTED_EDGE ( 'NONE', *, *, #19019, .T. ) ;
#10217=EDGE_CURVE ( 'NONE', #21173, #749, #11752, .T. ) ;
#10220=ADVANCED_FACE ( 'NONE', ( #11221 ), #11096, .T. ) ;
#10234=LINE ( 'NONE', #10016, #6117 ) ;
#10235=CARTESIAN_POINT ( 'NONE',  ( -3.806930669195367489, 0.7500000000000509592, -3.000000000000000444 ) ) ;
#10287=CARTESIAN_POINT ( 'NONE',  ( 4.690415759823415520, 0.7500000000000700551, -2.000000000000001776 ) ) ;
#10377=DIRECTION ( 'NONE',  ( -7.860214984770699307E-18, 1.409037165336591006E-16, 1.000000000000000000 ) ) ;
#10401=VERTEX_POINT ( 'NONE', #3644 ) ;
#10407=DIRECTION ( 'NONE',  ( 1.000000000000000000, -4.440892098500651800E-16, -7.860214984771115307E-18 ) ) ;
#10408=ORIENTED_EDGE ( 'NONE', *, *, #11736, .F. ) ;
#10453=ADVANCED_FACE ( 'NONE', ( #3748 ), #5532, .F. ) ;
#10630=STYLED_ITEM ( 'NONE', ( #19817 ), #10220 ) ;
#10748=ORIENTED_EDGE ( 'NONE', *, *, #20890, .F. ) ;
#10761=LINE ( 'NONE', #17950, #11177 ) ;
#10780=CARTESIAN_POINT ( 'NONE',  ( -2.500000000000000000, 2.761527815601792292E-14, -1.965053746193064019E-17 ) ) ;
#10842=CARTESIAN_POINT ( 'NONE',  ( 3.938275312863521282, -0.7499999999999389377, -2.974550175612221459 ) ) ;
#10965=ORIENTED_EDGE ( 'NONE', *, *, #4311, .F. ) ;
#11020=CARTESIAN_POINT ( 'NONE',  ( 1.387778780781445676E-14, 4.857225732735059864E-14, -1.500000000000001332 ) ) ;
#11096=CYLINDRICAL_SURFACE ( 'NONE', #1637, 2.499999999999993339 ) ;
#11105=EDGE_CURVE ( 'NONE', #16755, #5263, #21522, .T. ) ;
#11124=FACE_OUTER_BOUND ( 'NONE', #3659, .T. ) ;
#11173=SHAPE_DEFINITION_REPRESENTATION ( #10049, #16280 ) ;
#11177=VECTOR ( 'NONE', #23139, 1000.000000000000000 ) ;
#11179=VERTEX_POINT ( 'NONE', #11471 ) ;
#11221=FACE_OUTER_BOUND ( 'NONE', #12232, .T. ) ;
#11247=CARTESIAN_POINT ( 'NONE',  ( 0.000000000000000000, 1.387778780781445676E-14, 17.24999999999997513 ) ) ;
#11304=FILL_AREA_STYLE_COLOUR ( '', #17964 ) ;
#11342=AXIS2_PLACEMENT_3D ( 'NONE', #11247, #13139, #16308 ) ;
#11349=CIRCLE ( 'NONE', #3848, 2.499999999999993339 ) ;
#11396=CIRCLE ( 'NONE', #14417, 4.749999999999986677 ) ;
#11433=EDGE_LOOP ( 'NONE', ( #21693, #2184 ) ) ;
#11471=CARTESIAN_POINT ( 'NONE',  ( 3.674234614174737068, 0.7500000000000492939, -3.000000000000002665 ) ) ;
#11604=STYLED_ITEM ( 'NONE', ( #8171 ), #6953 ) ;
#11708=DIRECTION ( 'NONE',  ( -7.860214984770699307E-18, 1.409037165336591006E-16, 1.000000000000000000 ) ) ;
#11710=CARTESIAN_POINT ( 'NONE',  ( 1.387778780781445676E-14, 4.163336342344337027E-14, -2.000000000000001776 ) ) ;
#11734=CARTESIAN_POINT ( 'NONE',  ( 4.182608627552025560, 0.7500000000000556222, -2.876096987965587104 ) ) ;
#11736=EDGE_CURVE ( 'NONE', #7321, #919, #17777, .T. ) ;
#11752=CIRCLE ( 'NONE', #7630, 4.749999999999986677 ) ;
#11797=CARTESIAN_POINT ( 'NONE',  ( 4.163336342344337027E-14, 3.469446951953614189E-14, -3.000000000000002665 ) ) ;
#11852=EDGE_CURVE ( 'NONE', #4132, #955, #3179, .T. ) ;
#11876=EDGE_CURVE ( 'NONE', #919, #7321, #502, .T. ) ;
#11889=CARTESIAN_POINT ( 'NONE',  ( 4.750000000000013323, 3.286685320581564807E-14, -1.500000000000001332 ) ) ;
#12018=FACE_OUTER_BOUND ( 'NONE', #11433, .T. ) ;
#12030=( LENGTH_UNIT ( ) NAMED_UNIT ( * ) SI_UNIT ( .MILLI., .METRE. ) );
#12084=ADVANCED_FACE ( 'NONE', ( #3032 ), #8795, .T. ) ;
#12107=( GEOMETRIC_REPRESENTATION_CONTEXT ( 3 ) GLOBAL_UNCERTAINTY_ASSIGNED_CONTEXT ( ( #6269 ) ) GLOBAL_UNIT_ASSIGNED_CONTEXT ( ( #14842, #5805, #4013 ) ) REPRESENTATION_CONTEXT ( 'NONE', 'WORKASPACE' ) );
#12137=FACE_OUTER_BOUND ( 'NONE', #21477, .T. ) ;
#12148=ORIENTED_EDGE ( 'NONE', *, *, #11736, .T. ) ;
#12232=EDGE_LOOP ( 'NONE', ( #22789, #7792, #13011, #1040 ) ) ;
#12570=ADVANCED_FACE ( 'NONE', ( #7009 ), #21245, .F. ) ;
#12643=UNCERTAINTY_MEASURE_WITH_UNIT (LENGTH_MEASURE( 1.000000000000000082E-05 ), #8412, 'distance_accuracy_value', 'NONE');
#12651=VERTEX_POINT ( 'NONE', #10287 ) ;
#12714=ORIENTED_EDGE ( 'NONE', *, *, #4052, .T. ) ;
#12737=ORIENTED_EDGE ( 'NONE', *, *, #11876, .T. ) ;
#12743=ORIENTED_EDGE ( 'NONE', *, *, #20305, .F. ) ;
#12752=CIRCLE ( 'NONE', #6008, 4.749999999999986677 ) ;
#12756=( GEOMETRIC_REPRESENTATION_CONTEXT ( 3 ) GLOBAL_UNCERTAINTY_ASSIGNED_CONTEXT ( ( #13117 ) ) GLOBAL_UNIT_ASSIGNED_CONTEXT ( ( #12030, #886, #9818 ) ) REPRESENTATION_CONTEXT ( 'NONE', 'WORKASPACE' ) );
#12803=EDGE_CURVE ( 'NONE', #7321, #5263, #21594, .T. ) ;
#12944=PRODUCT_CONTEXT ( 'NONE', #15945, 'mechanical' ) ;
#12945=B_SPLINE_CURVE_WITH_KNOTS ( 'NONE', 3,
 ( #1197, #20612, #3073, #6484, #6377, #22490, #1317, #6604, #10235, #17290 ),
 .UNSPECIFIED., .F., .F.,
 ( 4, 2, 2, 2, 4 ),
 ( 0.005744585894170328028, 0.006138284319911526017, 0.006531982745652724007, 0.006925681171393922864, 0.007319379597135120853 ),
 .UNSPECIFIED. ) ;
#13011=ORIENTED_EDGE ( 'NONE', *, *, #5782, .T. ) ;
#13042=DIRECTION ( 'NONE',  ( 1.000000000000000000, -4.440892098500650814E-16, -7.860214984771113767E-18 ) ) ;
#13071=VECTOR ( 'NONE', #18549, 1000.000000000000000 ) ;
#13079=FILL_AREA_STYLE ('',( #14951 ) ) ;
#13117=UNCERTAINTY_MEASURE_WITH_UNIT (LENGTH_MEASURE( 1.000000000000000082E-05 ), #12030, 'distance_accuracy_value', 'NONE');
#13139=DIRECTION ( 'NONE',  ( 7.860214984770699307E-18, -1.409037165336591006E-16, -1.000000000000000000 ) ) ;
#13255=AXIS2_PLACEMENT_3D ( 'NONE', #1706, #8879, #10407 ) ;
#13274=AXIS2_PLACEMENT_3D ( 'NONE', #21683, #20137, #16240 ) ;
#13302=ORIENTED_EDGE ( 'NONE', *, *, #5652, .T. ) ;
#13421=CARTESIAN_POINT ( 'NONE',  ( -4.183059378720227706, -0.7499999999999437117, -2.875963052517019225 ) ) ;
#13457=DIRECTION ( 'NONE',  ( 1.000000000000000000, -4.440892098500650814E-16, -7.860214984771113767E-18 ) ) ;
#13524=EDGE_CURVE ( 'NONE', #12651, #4029, #12752, .T. ) ;
#13549=DIRECTION ( 'NONE',  ( -1.000000000000000000, 4.440892098500641939E-16, 0.000000000000000000 ) ) ;
#13605=FACE_OUTER_BOUND ( 'NONE', #18077, .T. ) ;
#13647=VECTOR ( 'NONE', #15629, 1000.000000000000000 ) ;
#13796=LINE ( 'NONE', #19326, #22666 ) ;
#13821=ORIENTED_EDGE ( 'NONE', *, *, #10028, .T. ) ;
#13842=EDGE_LOOP ( 'NONE', ( #18391, #22342 ) ) ;
#13889=FACE_OUTER_BOUND ( 'NONE', #6495, .T. ) ;
#13911=CARTESIAN_POINT ( 'NONE',  ( 2.500000000000000000, 2.570099380655439722E-14, 17.24999999999997513 ) ) ;
#13961=EDGE_CURVE ( 'NONE', #21586, #955, #16525, .T. ) ;
#14008=( NAMED_UNIT ( * ) SI_UNIT ( $, .STERADIAN. ) SOLID_ANGLE_UNIT ( ) );
#14051=EDGE_LOOP ( 'NONE', ( #17037, #5548 ) ) ;
#14122=CARTESIAN_POINT ( 'NONE',  ( 0.000000000000000000, 2.775557561562891351E-14, 17.49999999999997513 ) ) ;
#14125=ADVANCED_FACE ( 'NONE', ( #12137 ), #22940, .T. ) ;
#14165=VECTOR ( 'NONE', #21223, 1000.000000000000000 ) ;
#14226=CARTESIAN_POINT ( 'NONE',  ( -4.690415759823429731, -0.7499999999999520384, -2.999999999999995559 ) ) ;
#14228=ORIENTED_EDGE ( 'NONE', *, *, #4213, .T. ) ;
#14235=CARTESIAN_POINT ( 'NONE',  ( 5.213674118230995802, 0.7500000000000561773, -1.500000000000001332 ) ) ;
#14265=CARTESIAN_POINT ( 'NONE',  ( 4.690415759823637565, -0.7499999999999382716, -2.000000000000029310 ) ) ;
#14302=CARTESIAN_POINT ( 'NONE',  ( -4.690415759823443942, 0.7500000000000770495, -2.000000000000001776 ) ) ;
#14397=VERTEX_POINT ( 'NONE', #16807 ) ;
#14415=CARTESIAN_POINT ( 'NONE',  ( 4.690415759823373776, -0.7499999999999382716, -1.500000000000001332 ) ) ;
#14417=AXIS2_PLACEMENT_3D ( 'NONE', #11020, #14667, #439 ) ;
#14444=B_SPLINE_CURVE_WITH_KNOTS ( 'NONE', 3,
 ( #4098, #584, #6108, #11734, #15153, #18681, #5997, #16906, #9631, #4322 ),
 .UNSPECIFIED., .F., .F.,
 ( 4, 2, 2, 2, 4 ),
 ( 0.001114109625932955920, 0.001508381724359308257, 0.001902653822785660810, 0.002296925921212013364, 0.002691198019638365701 ),
 .UNSPECIFIED. ) ;
#14611=FACE_OUTER_BOUND ( 'NONE', #22765, .T. ) ;
#14667=DIRECTION ( 'NONE',  ( -7.860214984770699307E-18, 1.409037165336591006E-16, 1.000000000000000000 ) ) ;
#14719=SURFACE_STYLE_USAGE ( .BOTH. , #22375 ) ;
#14774=DIRECTION ( 'NONE',  ( 7.860214984770699307E-18, -1.409037165336591006E-16, -1.000000000000000000 ) ) ;
#14791=EDGE_CURVE ( 'NONE', #11179, #12651, #14444, .T. ) ;
#14804=DIRECTION ( 'NONE',  ( -7.860214984770699307E-18, 1.409037165336591006E-16, 1.000000000000000000 ) ) ;
#14842=( LENGTH_UNIT ( ) NAMED_UNIT ( * ) SI_UNIT ( .MILLI., .METRE. ) );
#14857=EDGE_LOOP ( 'NONE', ( #1972, #17533, #7995, #13821 ) ) ;
#14864=( LENGTH_UNIT ( ) NAMED_UNIT ( * ) SI_UNIT ( .MILLI., .METRE. ) );
#14917=VECTOR ( 'NONE', #6965, 1000.000000000000000 ) ;
#14929=AXIS2_PLACEMENT_3D ( 'NONE', #15209, #2747, #15442 ) ;
#14951=FILL_AREA_STYLE_COLOUR ( '', #9121 ) ;
#15039=AXIS2_PLACEMENT_3D ( 'NONE', #17797, #1678, #3218 ) ;
#15062=CARTESIAN_POINT ( 'NONE',  ( 4.690415759823637565, -0.7499999999999382716, -2.000000000000029310 ) ) ;
#15153=CARTESIAN_POINT ( 'NONE',  ( 4.296135882448235854, 0.7500000000000558442, -2.802242829034434557 ) ) ;
#15174=CARTESIAN_POINT ( 'NONE',  ( -4.294683695178314942, -0.7499999999999437117, -2.803608044185096126 ) ) ;
#15184=SURFACE_SIDE_STYLE ('',( #16935 ) ) ;
#15209=CARTESIAN_POINT ( 'NONE',  ( 4.163336342344337027E-14, 3.469446951953614189E-14, -3.000000000000002665 ) ) ;
#15373=DIRECTION ( 'NONE',  ( -1.000000000000000000, 4.440892098500637995E-16, 0.000000000000000000 ) ) ;
#15400=ADVANCED_FACE ( 'NONE', ( #14611 ), #4123, .T. ) ;
#15442=DIRECTION ( 'NONE',  ( 1.000000000000000000, -4.440892098500658702E-16, 0.000000000000000000 ) ) ;
#15596=CIRCLE ( 'NONE', #9595, 4.749999999999986677 ) ;
#15629=DIRECTION ( 'NONE',  ( -7.860214984770699307E-18, 1.409037165336591006E-16, 1.000000000000000000 ) ) ;
#15659=LINE ( 'NONE', #8732, #14165 ) ;
#15735=DIRECTION ( 'NONE',  ( 7.860214984770699307E-18, -1.409037165336591006E-16, -1.000000000000000000 ) ) ;
#15762=DIRECTION ( 'NONE',  ( 1.000000000000000000, -4.440892098500651800E-16, -7.860214984771115307E-18 ) ) ;
#15781=DIRECTION ( 'NONE',  ( 7.860214984771176937E-18, 1.409037165336591006E-16, 1.000000000000000000 ) ) ;
#15860=EDGE_LOOP ( 'NONE', ( #1208, #10050, #19632, #3242, #9336, #9535 ) ) ;
#15867=PLANE ( 'NONE',  #1671 ) ;
#15893=CARTESIAN_POINT ( 'NONE',  ( 4.663920909892617317, -0.7499999999999384936, -2.263164618243533432 ) ) ;
#15926=CLOSED_SHELL ( 'NONE', ( #14125, #10220, #15400, #19594, #19134, #4506, #12570, #15994, #20613, #6835, #18562, #9770, #10453, #18324, #12084 ) ) ;
#15945=APPLICATION_CONTEXT ( 'automotive_design' ) ;
#15994=ADVANCED_FACE ( 'NONE', ( #20573, #5993 ), #20336, .T. ) ;
#16001=ORIENTED_EDGE ( 'NONE', *, *, #13524, .F. ) ;
#16208=AXIS2_PLACEMENT_3D ( 'NONE', #20022, #9203, #19588 ) ;
#16240=DIRECTION ( 'NONE',  ( 1.000000000000000000, -4.440892098500651800E-16, 0.000000000000000000 ) ) ;
#16271=CARTESIAN_POINT ( 'NONE',  ( 0.000000000000000000, 0.000000000000000000, 0.000000000000000000 ) ) ;
#16280=SHAPE_REPRESENTATION ( 'Bolt', ( #22115 ), #22911 ) ;
#16293=APPLICATION_CONTEXT ( 'automotive_design' ) ;
#16303=DIRECTION ( 'NONE',  ( 6.106226635438366889E-16, -1.000000000000000000, 1.409037165336591006E-16 ) ) ;
#16308=DIRECTION ( 'NONE',  ( 1.000000000000000000, -4.440892098500654758E-16, 0.000000000000000000 ) ) ;
#16483=DIRECTION ( 'NONE',  ( 1.000000000000000000, -4.440892098500654758E-16, 0.000000000000000000 ) ) ;
#16525=CIRCLE ( 'NONE', #16899, 4.749999999999986677 ) ;
#16554=CARTESIAN_POINT ( 'NONE',  ( 5.213674118231010013, -0.7499999999999520384, -2.999999999999995559 ) ) ;
#16631=MECHANICAL_DESIGN_GEOMETRIC_PRESENTATION_REPRESENTATION('',(#10630),#4234);
#16755=VERTEX_POINT ( 'NONE', #13911 ) ;
#16777=CARTESIAN_POINT ( 'NONE',  ( -4.690415759823415520, -0.7499999999999382716, -1.500000000000001332 ) ) ;
#16807=CARTESIAN_POINT ( 'NONE',  ( 3.674234614174737068, -0.7499999999999451550, -3.000000000000002665 ) ) ;
#16840=EDGE_CURVE ( 'NONE', #12651, #10401, #13796, .T. ) ;
#16858=EDGE_CURVE ( 'NONE', #23243, #14397, #5941, .T. ) ;
#16899=AXIS2_PLACEMENT_3D ( 'NONE', #4502, #20869, #18628 ) ;
#16906=CARTESIAN_POINT ( 'NONE',  ( 4.663380343546485562, 0.7500000000000558442, -2.264472787102512985 ) ) ;
#16935=SURFACE_STYLE_FILL_AREA ( #9666 ) ;
#17011=CARTESIAN_POINT ( 'NONE',  ( 0.000000000000000000, 2.775557561562891351E-14, 17.49999999999997513 ) ) ;
#17020=CARTESIAN_POINT ( 'NONE',  ( 0.000000000000000000, 0.000000000000000000, 0.000000000000000000 ) ) ;
#17037=ORIENTED_EDGE ( 'NONE', *, *, #10028, .F. ) ;
#17056=LINE ( 'NONE', #22598, #7323 ) ;
#17177=DIRECTION ( 'NONE',  ( 7.860214984770699307E-18, -1.409037165336591006E-16, -1.000000000000000000 ) ) ;
#17290=CARTESIAN_POINT ( 'NONE',  ( -3.674234614174765046, 0.7500000000000630607, -2.999999999999995559 ) ) ;
#17433=EDGE_CURVE ( 'NONE', #14397, #19077, #9410, .T. ) ;
#17504=ORIENTED_EDGE ( 'NONE', *, *, #3827, .F. ) ;
#17520=AXIS2_PLACEMENT_3D ( 'NONE', #18150, #5907, #5685 ) ;
#17531=AXIS2_PLACEMENT_3D ( 'NONE', #6383, #6810, #9784 ) ;
#17533=ORIENTED_EDGE ( 'NONE', *, *, #11105, .T. ) ;
#17648=( LENGTH_UNIT ( ) NAMED_UNIT ( * ) SI_UNIT ( .MILLI., .METRE. ) );
#17683=VERTEX_POINT ( 'NONE', #14415 ) ;
#17719=ORIENTED_EDGE ( 'NONE', *, *, #21026, .F. ) ;
#17777=CIRCLE ( 'NONE', #13274, 2.249999999999996003 ) ;
#17794=VECTOR ( 'NONE', #4099, 1000.000000000000000 ) ;
#17797=CARTESIAN_POINT ( 'NONE',  ( 0.000000000000000000, 2.775557561562891351E-14, 17.49999999999997513 ) ) ;
#17881=DIRECTION ( 'NONE',  ( -7.860214984770699307E-18, 1.409037165336591006E-16, 1.000000000000000000 ) ) ;
#17927=ORIENTED_EDGE ( 'NONE', *, *, #13524, .T. ) ;
#17933=CIRCLE ( 'NONE', #17531, 4.749999999999986677 ) ;
#17938=FILL_AREA_STYLE_COLOUR ( '', #500 ) ;
#17950=CARTESIAN_POINT ( 'NONE',  ( 5.213674118230995802, 0.7500000000000561773, -1.500000000000001332 ) ) ;
#17961=ORIENTED_EDGE ( 'NONE', *, *, #19019, .F. ) ;
#17964=COLOUR_RGB ( '', 0.08235294, 0.09019608, 0.10196078) ;
#18077=EDGE_LOOP ( 'NONE', ( #10748, #16001, #19392, #10965 ) ) ;
#18150=CARTESIAN_POINT ( 'NONE',  ( 4.163336342344337027E-14, 3.469446951953614189E-14, -3.000000000000002665 ) ) ;
#18178=DIRECTION ( 'NONE',  ( 7.860214984770699307E-18, -1.409037165336591006E-16, -1.000000000000000000 ) ) ;
#18309=EDGE_CURVE ( 'NONE', #5263, #9570, #17056, .T. ) ;
#18324=ADVANCED_FACE ( 'NONE', ( #13889 ), #6375, .T. ) ;
#18370=CARTESIAN_POINT ( 'NONE',  ( -3.937547562846346327, -0.7499999999999433786, -2.974837901130639395 ) ) ;
#18391=ORIENTED_EDGE ( 'NONE', *, *, #10217, .T. ) ;
#18549=DIRECTION ( 'NONE',  ( 7.860214984770699307E-18, -1.409037165336591006E-16, -1.000000000000000000 ) ) ;
#18562=ADVANCED_FACE ( 'NONE', ( #8711 ), #15867, .T. ) ;
#18600=CARTESIAN_POINT ( 'NONE',  ( -3.674234614174765046, -0.7499999999999451550, -3.000000000000051070 ) ) ;
#18628=DIRECTION ( 'NONE',  ( -1.000000000000000000, -2.220446049250311109E-15, 0.000000000000000000 ) ) ;
#18634=CARTESIAN_POINT ( 'NONE',  ( -4.690415759824456465, -0.7499999999999242828, -1.999999999999849010 ) ) ;
#18681=CARTESIAN_POINT ( 'NONE',  ( 4.484160662959468802, 0.7500000000000558442, -2.618649729759251699 ) ) ;
#18684=DIRECTION ( 'NONE',  ( 1.000000000000000000, -4.440892098500650814E-16, -7.860214984771115307E-18 ) ) ;
#18690=CIRCLE ( 'NONE', #14929, 3.749999999999989786 ) ;
#18741=VECTOR ( 'NONE', #3015, 1000.000000000000000 ) ;
#18899=DIRECTION ( 'NONE',  ( 1.000000000000000000, -4.440892098500655744E-16, 7.860214984770760936E-18 ) ) ;
#18931=CARTESIAN_POINT ( 'NONE',  ( 0.000000000000000000, 0.000000000000000000, 0.000000000000000000 ) ) ;
#18954=EDGE_CURVE ( 'NONE', #16755, #6059, #1395, .T. ) ;
#18959=DIRECTION ( 'NONE',  ( -7.860214984771176937E-18, -1.409037165336591006E-16, -1.000000000000000000 ) ) ;
#19019=EDGE_CURVE ( 'NONE', #6944, #10401, #11396, .T. ) ;
#19069=DIRECTION ( 'NONE',  ( 0.7071067811865435759, -3.270568595685441704E-16, -0.7071067811865514585 ) ) ;
#19077=VERTEX_POINT ( 'NONE', #5741 ) ;
#19079=VECTOR ( 'NONE', #20988, 1000.000000000000000 ) ;
#19124=LINE ( 'NONE', #22663, #18741 ) ;
#19134=ADVANCED_FACE ( 'NONE', ( #22083 ), #19294, .T. ) ;
#19197=TOROIDAL_SURFACE ( 'NONE', #9057, 3.750000000000000000, 1.000000000000000000 ) ;
#19217=( NAMED_UNIT ( * ) SI_UNIT ( $, .STERADIAN. ) SOLID_ANGLE_UNIT ( ) );
#19245=AXIS2_PLACEMENT_3D ( 'NONE', #95, #16303, #14774 ) ;
#19294=TOROIDAL_SURFACE ( 'NONE', #21582, 3.750000000000000000, 1.000000000000000000 ) ;
#19326=CARTESIAN_POINT ( 'NONE',  ( 4.690415759823387987, 0.7500000000000492939, -3.000000000000002665 ) ) ;
#19392=ORIENTED_EDGE ( 'NONE', *, *, #14791, .F. ) ;
#19447=PRODUCT ( 'Bolt', 'Bolt', '', ( #12944 ) ) ;
#19461=DIRECTION ( 'NONE',  ( 7.860214984771176937E-18, 1.409037165336591006E-16, 1.000000000000000000 ) ) ;
#19526=ORIENTED_EDGE ( 'NONE', *, *, #13961, .F. ) ;
#19533=DIRECTION ( 'NONE',  ( 1.000000000000000000, -4.440892098500650814E-16, -7.860214984771113767E-18 ) ) ;
#19588=DIRECTION ( 'NONE',  ( 1.000000000000000000, -4.440892098500654758E-16, 0.000000000000000000 ) ) ;
#19594=ADVANCED_FACE ( 'NONE', ( #12018 ), #1445, .F. ) ;
#19616=CARTESIAN_POINT ( 'NONE',  ( 4.163336342344337027E-14, 3.469446951953614189E-14, -3.000000000000002665 ) ) ;
#19632=ORIENTED_EDGE ( 'NONE', *, *, #1371, .T. ) ;
#19678=CARTESIAN_POINT ( 'NONE',  ( 4.182403429330263656, -0.7499999999999387157, -2.876221860228560967 ) ) ;
#19699=ORIENTED_EDGE ( 'NONE', *, *, #11105, .F. ) ;
#19817=PRESENTATION_STYLE_ASSIGNMENT (( #2043 ) ) ;
#19985=ORIENTED_EDGE ( 'NONE', *, *, #4722, .F. ) ;
#20022=CARTESIAN_POINT ( 'NONE',  ( 4.163336342344337027E-14, 3.469446951953614189E-14, -3.000000000000002665 ) ) ;
#20115=CARTESIAN_POINT ( 'NONE',  ( 2.500000000000000000, 2.570099380655443508E-14, 1.965053746192312752E-17 ) ) ;
#20121=EDGE_LOOP ( 'NONE', ( #17504, #3385, #744, #9456, #3209, #20661, #14228, #12743 ) ) ;
#20122=PRODUCT_DEFINITION ( 'UNKNOWN', '', #10, #2752 ) ;
#20131=CARTESIAN_POINT ( 'NONE',  ( -4.690415759824456465, -0.7499999999999242828, -1.999999999999849010 ) ) ;
#20137=DIRECTION ( 'NONE',  ( -7.860214984770699307E-18, 1.409037165336591006E-16, 1.000000000000000000 ) ) ;
#20230=( GEOMETRIC_REPRESENTATION_CONTEXT ( 3 ) GLOBAL_UNCERTAINTY_ASSIGNED_CONTEXT ( ( #7455 ) ) GLOBAL_UNIT_ASSIGNED_CONTEXT ( ( #17648, #3316, #14008 ) ) REPRESENTATION_CONTEXT ( 'NONE', 'WORKASPACE' ) );
#20264=SURFACE_STYLE_FILL_AREA ( #13079 ) ;
#20300=ORIENTED_EDGE ( 'NONE', *, *, #16858, .T. ) ;
#20305=EDGE_CURVE ( 'NONE', #749, #21173, #15596, .T. ) ;
#20336=PLANE ( 'NONE',  #1579 ) ;
#20573=FACE_BOUND ( 'NONE', #14051, .T. ) ;
#20612=CARTESIAN_POINT ( 'NONE',  ( -4.690415759823418185, 0.7500000000000500711, -2.132253920548287773 ) ) ;
#20613=ADVANCED_FACE ( 'NONE', ( #13605 ), #19197, .T. ) ;
#20645=MECHANICAL_DESIGN_GEOMETRIC_PRESENTATION_REPRESENTATION('',(#11604),#12756);
#20653=SURFACE_SIDE_STYLE ('',( #6297 ) ) ;
#20661=ORIENTED_EDGE ( 'NONE', *, *, #950, .T. ) ;
#20678=CARTESIAN_POINT ( 'NONE',  ( -4.749999999999985789, 3.766740792898615283E-14, -1.500000000000001332 ) ) ;
#20704=CARTESIAN_POINT ( 'NONE',  ( -2.250000000000001776, 2.879267452445610575E-14, 17.49999999999997513 ) ) ;
#20869=DIRECTION ( 'NONE',  ( -7.860214984770699307E-18, 1.409037165336591006E-16, 1.000000000000000000 ) ) ;
#20886=ORIENTED_EDGE ( 'NONE', *, *, #16840, .F. ) ;
#20890=EDGE_CURVE ( 'NONE', #4029, #5959, #12945, .T. ) ;
#20894=DIRECTION ( 'NONE',  ( 1.000000000000000000, -4.440892098500654758E-16, 0.000000000000000000 ) ) ;
#20957=DIRECTION ( 'NONE',  ( -1.000000000000000000, 4.440892098500650814E-16, 7.860214984771113767E-18 ) ) ;
#20974=CIRCLE ( 'NONE', #1423, 4.749999999999986677 ) ;
#20988=DIRECTION ( 'NONE',  ( -7.860214984770699307E-18, 1.409037165336591006E-16, 1.000000000000000000 ) ) ;
#20995=SURFACE_STYLE_USAGE ( .BOTH. , #20653 ) ;
#21026=EDGE_CURVE ( 'NONE', #3456, #4029, #3756, .T. ) ;
#21073=DIRECTION ( 'NONE',  ( 7.860214984770699307E-18, -1.409037165336591006E-16, -1.000000000000000000 ) ) ;
#21173=VERTEX_POINT ( 'NONE', #3170 ) ;
#21223=DIRECTION ( 'NONE',  ( 1.000000000000000000, -4.440892098500650814E-16, -7.860214984771115307E-18 ) ) ;
#21245=PLANE ( 'NONE',  #2798 ) ;
#21310=DIRECTION ( 'NONE',  ( 7.860214984771176937E-18, 1.409037165336591006E-16, 1.000000000000000000 ) ) ;
#21323=CIRCLE ( 'NONE', #23156, 3.749999999999989786 ) ;
#21354=SHAPE_REPRESENTATION_RELATIONSHIP ( 'NONE' , 'NONE' ,  #16280, #6953 ) ;
#21362=ORIENTED_EDGE ( 'NONE', *, *, #12803, .T. ) ;
#21454=CARTESIAN_POINT ( 'NONE',  ( 3.674234614174737068, -0.7499999999999451550, -3.000000000000002665 ) ) ;
#21477=EDGE_LOOP ( 'NONE', ( #5896, #13302, #21557, #1716 ) ) ;
#21522=CIRCLE ( 'NONE', #11342, 2.499999999999993339 ) ;
#21557=ORIENTED_EDGE ( 'NONE', *, *, #5591, .F. ) ;
#21582=AXIS2_PLACEMENT_3D ( 'NONE', #11710, #8075, #4540 ) ;
#21586=VERTEX_POINT ( 'NONE', #20678 ) ;
#21594=LINE ( 'NONE', #9107, #9566 ) ;
#21595=SURFACE_STYLE_FILL_AREA ( #4037 ) ;
#21648=CARTESIAN_POINT ( 'NONE',  ( -4.750000000000000000, 3.766740792898668295E-14, -3.733602117766605407E-17 ) ) ;
#21683=CARTESIAN_POINT ( 'NONE',  ( 0.000000000000000000, 2.775557561562891351E-14, 17.49999999999997513 ) ) ;
#21693=ORIENTED_EDGE ( 'NONE', *, *, #4722, .T. ) ;
#21705=CARTESIAN_POINT ( 'NONE',  ( 0.000000000000000000, 2.775557561562891351E-14, 17.49999999999997513 ) ) ;
#21782=EDGE_LOOP ( 'NONE', ( #12148, #12737 ) ) ;
#21820=SURFACE_SIDE_STYLE ('',( #21595 ) ) ;
#21908=PRESENTATION_STYLE_ASSIGNMENT (( #14719 ) ) ;
#21930=ORIENTED_EDGE ( 'NONE', *, *, #1687, .T. ) ;
#22082=CARTESIAN_POINT ( 'NONE',  ( 4.690415759823387987, -0.7499999999999520384, -3.000000000000002665 ) ) ;
#22083=FACE_OUTER_BOUND ( 'NONE', #2495, .T. ) ;
#22115=AXIS2_PLACEMENT_3D ( 'NONE', #4943, #2963, #5306 ) ;
#22173=ORIENTED_EDGE ( 'NONE', *, *, #3827, .T. ) ;
#22186=EDGE_CURVE ( 'NONE', #3456, #21586, #17933, .T. ) ;
#22284=CARTESIAN_POINT ( 'NONE',  ( 4.750000000000028422, 3.258504577274833815E-14, -3.000000000000002665 ) ) ;
#22342=ORIENTED_EDGE ( 'NONE', *, *, #20305, .T. ) ;
#22368=CARTESIAN_POINT ( 'NONE',  ( -4.690415759823517661, -0.7499999999999440448, -2.263420659773247579 ) ) ;
#22375=SURFACE_SIDE_STYLE ('',( #20264 ) ) ;
#22379=PRESENTATION_STYLE_ASSIGNMENT (( #2712 ) ) ;
#22475=CIRCLE ( 'NONE', #6341, 2.499999999999993339 ) ;
#22489=CARTESIAN_POINT ( 'NONE',  ( 0.000000000000000000, 0.000000000000000000, 0.000000000000000000 ) ) ;
#22490=CARTESIAN_POINT ( 'NONE',  ( -4.295732246213650463, 0.7500000000000505151, -2.802538081657628410 ) ) ;
#22598=CARTESIAN_POINT ( 'NONE',  ( -2.499999999999993339, 2.886579864025407005E-14, 17.49999999999997513 ) ) ;
#22663=CARTESIAN_POINT ( 'NONE',  ( -4.749999999999944933, 3.738560049591893758E-14, -3.000000000000002665 ) ) ;
#22666=VECTOR ( 'NONE', #10377, 1000.000000000000000 ) ;
#22765=EDGE_LOOP ( 'NONE', ( #8351, #22173, #4085, #1300, #10142, #20886, #17927, #17719 ) ) ;
#22789=ORIENTED_EDGE ( 'NONE', *, *, #5591, .T. ) ;
#22819=CARTESIAN_POINT ( 'NONE',  ( 0.000000000000000000, 2.775557561562891351E-14, 17.49999999999997513 ) ) ;
#22911=( GEOMETRIC_REPRESENTATION_CONTEXT ( 3 ) GLOBAL_UNCERTAINTY_ASSIGNED_CONTEXT ( ( #12643 ) ) GLOBAL_UNIT_ASSIGNED_CONTEXT ( ( #8412, #2996, #19217 ) ) REPRESENTATION_CONTEXT ( 'NONE', 'WORKASPACE' ) );
#22932=CARTESIAN_POINT ( 'NONE',  ( 2.499999999999993339, 2.695151429079059169E-14, 17.49999999999997513 ) ) ;
#22940=CONICAL_SURFACE ( 'NONE', #15039, 2.249999999999996003, 0.7853981633974439491 ) ;
#22978=CARTESIAN_POINT ( 'NONE',  ( 4.295266925971481520, -0.7499999999999386047, -2.803037596611578586 ) ) ;
#23030=EDGE_CURVE ( 'NONE', #4132, #23243, #20974, .T. ) ;
#23043=DIRECTION ( 'NONE',  ( 1.000000000000000000, -4.440892098500658702E-16, 0.000000000000000000 ) ) ;
#23139=DIRECTION ( 'NONE',  ( 1.000000000000000000, -4.440892098500650814E-16, -7.860214984771115307E-18 ) ) ;
#23156=AXIS2_PLACEMENT_3D ( 'NONE', #19616, #8249, #23043 ) ;
#23243=VERTEX_POINT ( 'NONE', #15062 ) ;
ENDSEC;
END-ISO-10303-21;
